ISO-10303-21;
HEADER;
/* Generated by software containing ST-Developer
 * from STEP Tools, Inc. (www.steptools.com) 
 */

FILE_DESCRIPTION(
/* description */ ('PAT-041'),
/* implementation_level */ '2;1');

FILE_NAME(
/* name */ 'Hex Nut - M8.step',
/* time_stamp */ '2026-10-28T22:21:24-07:00',
/* author */ (''),
/* organization */ (''),
/* preprocessor_version */ 'ST-DEVELOPER v20.2',
/* originating_system */ 'Autodesk Translation Framework v15.17.0.0',
/* authorisation */ '');

FILE_SCHEMA (('AUTOMOTIVE_DESIGN { 1 0 10303 214 3 1 1 }'));
ENDSEC;

DATA;
#10=MECHANICAL_DESIGN_GEOMETRIC_PRESENTATION_REPRESENTATION('',(#218),#2507);
#173=(
BOUNDED_CURVE()
B_SPLINE_CURVE(2,(#2372,#2373,#2374),.UNSPECIFIED.,.F.,.F.)
B_SPLINE_CURVE_WITH_KNOTS((3,3),(0.14973948338295,0.97160236658079),
 .UNSPECIFIED.)
CURVE()
GEOMETRIC_REPRESENTATION_ITEM()
RATIONAL_B_SPLINE_CURVE((1.07140024848292,1.23714644374248,1.07140024848292))
REPRESENTATION_ITEM('')
);
#174=(
BOUNDED_CURVE()
B_SPLINE_CURVE(2,(#2376,#2377,#2378),.UNSPECIFIED.,.F.,.F.)
B_SPLINE_CURVE_WITH_KNOTS((3,3),(0.14973948338295,0.971602366580789),
 .UNSPECIFIED.)
CURVE()
GEOMETRIC_REPRESENTATION_ITEM()
RATIONAL_B_SPLINE_CURVE((1.07140024848292,1.23714644374248,1.07140024848292))
REPRESENTATION_ITEM('')
);
#175=(
BOUNDED_CURVE()
B_SPLINE_CURVE(2,(#2383,#2384,#2385),.UNSPECIFIED.,.F.,.F.)
B_SPLINE_CURVE_WITH_KNOTS((3,3),(0.14973948338295,0.97160236658079),
 .UNSPECIFIED.)
CURVE()
GEOMETRIC_REPRESENTATION_ITEM()
RATIONAL_B_SPLINE_CURVE((1.07140024848292,1.23714644374248,1.07140024848292))
REPRESENTATION_ITEM('')
);
#176=(
BOUNDED_CURVE()
B_SPLINE_CURVE(2,(#2387,#2388,#2389),.UNSPECIFIED.,.F.,.F.)
B_SPLINE_CURVE_WITH_KNOTS((3,3),(0.14973948338295,0.97160236658079),
 .UNSPECIFIED.)
CURVE()
GEOMETRIC_REPRESENTATION_ITEM()
RATIONAL_B_SPLINE_CURVE((1.07140024848292,1.23714644374248,1.07140024848292))
REPRESENTATION_ITEM('')
);
#177=(
BOUNDED_CURVE()
B_SPLINE_CURVE(2,(#2391,#2392,#2393),.UNSPECIFIED.,.F.,.F.)
B_SPLINE_CURVE_WITH_KNOTS((3,3),(0.14973948338295,0.971602366580789),
 .UNSPECIFIED.)
CURVE()
GEOMETRIC_REPRESENTATION_ITEM()
RATIONAL_B_SPLINE_CURVE((1.07140024848292,1.23714644374248,1.07140024848292))
REPRESENTATION_ITEM('')
);
#178=(
BOUNDED_CURVE()
B_SPLINE_CURVE(2,(#2394,#2395,#2396),.UNSPECIFIED.,.F.,.F.)
B_SPLINE_CURVE_WITH_KNOTS((3,3),(0.14973948338295,0.97160236658079),
 .UNSPECIFIED.)
CURVE()
GEOMETRIC_REPRESENTATION_ITEM()
RATIONAL_B_SPLINE_CURVE((1.07140024848292,1.23714644374248,1.07140024848292))
REPRESENTATION_ITEM('')
);
#179=(
BOUNDED_CURVE()
B_SPLINE_CURVE(2,(#2403,#2404,#2405),.UNSPECIFIED.,.F.,.F.)
B_SPLINE_CURVE_WITH_KNOTS((3,3),(0.14973948338295,0.97160236658079),
 .UNSPECIFIED.)
CURVE()
GEOMETRIC_REPRESENTATION_ITEM()
RATIONAL_B_SPLINE_CURVE((1.07140024848292,1.23714644374248,1.07140024848292))
REPRESENTATION_ITEM('')
);
#180=(
BOUNDED_CURVE()
B_SPLINE_CURVE(2,(#2407,#2408,#2409),.UNSPECIFIED.,.F.,.F.)
B_SPLINE_CURVE_WITH_KNOTS((3,3),(0.14973948338295,0.97160236658079),
 .UNSPECIFIED.)
CURVE()
GEOMETRIC_REPRESENTATION_ITEM()
RATIONAL_B_SPLINE_CURVE((1.07140024848292,1.23714644374248,1.07140024848292))
REPRESENTATION_ITEM('')
);
#181=(
BOUNDED_CURVE()
B_SPLINE_CURVE(2,(#2411,#2412,#2413),.UNSPECIFIED.,.F.,.F.)
B_SPLINE_CURVE_WITH_KNOTS((3,3),(0.14973948338295,0.971602366580789),
 .UNSPECIFIED.)
CURVE()
GEOMETRIC_REPRESENTATION_ITEM()
RATIONAL_B_SPLINE_CURVE((1.07140024848292,1.23714644374248,1.07140024848292))
REPRESENTATION_ITEM('')
);
#182=(
BOUNDED_CURVE()
B_SPLINE_CURVE(2,(#2415,#2416,#2417),.UNSPECIFIED.,.F.,.F.)
B_SPLINE_CURVE_WITH_KNOTS((3,3),(0.14973948338295,0.97160236658079),
 .UNSPECIFIED.)
CURVE()
GEOMETRIC_REPRESENTATION_ITEM()
RATIONAL_B_SPLINE_CURVE((1.07140024848292,1.23714644374248,1.07140024848292))
REPRESENTATION_ITEM('')
);
#183=(
BOUNDED_CURVE()
B_SPLINE_CURVE(2,(#2419,#2420,#2421),.UNSPECIFIED.,.F.,.F.)
B_SPLINE_CURVE_WITH_KNOTS((3,3),(0.14973948338295,0.97160236658079),
 .UNSPECIFIED.)
CURVE()
GEOMETRIC_REPRESENTATION_ITEM()
RATIONAL_B_SPLINE_CURVE((1.07140024848292,1.23714644374248,1.07140024848292))
REPRESENTATION_ITEM('')
);
#184=(
BOUNDED_CURVE()
B_SPLINE_CURVE(2,(#2422,#2423,#2424),.UNSPECIFIED.,.F.,.F.)
B_SPLINE_CURVE_WITH_KNOTS((3,3),(0.14973948338295,0.971602366580789),
 .UNSPECIFIED.)
CURVE()
GEOMETRIC_REPRESENTATION_ITEM()
RATIONAL_B_SPLINE_CURVE((1.07140024848292,1.23714644374248,1.07140024848292))
REPRESENTATION_ITEM('')
);
#187=CONICAL_SURFACE('',#1589,0.734027674973257,1.0471975511966);
#188=CONICAL_SURFACE('',#1591,0.734027674973257,1.0471975511966);
#198=SHAPE_REPRESENTATION_RELATIONSHIP('SRR','None',#2583,#208);
#208=ADVANCED_BREP_SHAPE_REPRESENTATION('',(#228),#2506);
#218=STYLED_ITEM('',(#2701),#228);
#228=MANIFOLD_SOLID_BREP('Body1',#1338);
#278=FACE_BOUND('',#503,.T.);
#279=FACE_BOUND('',#505,.T.);
#305=PLANE('',#1593);
#306=PLANE('',#1594);
#307=PLANE('',#1595);
#308=PLANE('',#1599);
#309=PLANE('',#1600);
#310=PLANE('',#1601);
#311=PLANE('',#1602);
#312=PLANE('',#1603);
#373=FACE_OUTER_BOUND('',#493,.T.);
#374=FACE_OUTER_BOUND('',#494,.T.);
#375=FACE_OUTER_BOUND('',#495,.T.);
#376=FACE_OUTER_BOUND('',#496,.T.);
#377=FACE_OUTER_BOUND('',#497,.T.);
#378=FACE_OUTER_BOUND('',#498,.T.);
#379=FACE_OUTER_BOUND('',#499,.T.);
#380=FACE_OUTER_BOUND('',#500,.T.);
#381=FACE_OUTER_BOUND('',#501,.T.);
#382=FACE_OUTER_BOUND('',#502,.T.);
#383=FACE_OUTER_BOUND('',#504,.T.);
#493=EDGE_LOOP('',(#1174,#1175,#1176,#1177,#1178,#1179,#1180,#1181,#1182));
#494=EDGE_LOOP('',(#1183,#1184,#1185,#1186,#1187,#1188,#1189,#1190,#1191));
#495=EDGE_LOOP('',(#1192,#1193,#1194,#1195));
#496=EDGE_LOOP('',(#1196,#1197,#1198,#1199));
#497=EDGE_LOOP('',(#1200,#1201,#1202,#1203));
#498=EDGE_LOOP('',(#1204,#1205,#1206,#1207));
#499=EDGE_LOOP('',(#1208,#1209,#1210,#1211));
#500=EDGE_LOOP('',(#1212,#1213,#1214,#1215));
#501=EDGE_LOOP('',(#1216,#1217,#1218,#1219));
#502=EDGE_LOOP('',(#1220));
#503=EDGE_LOOP('',(#1221));
#504=EDGE_LOOP('',(#1222));
#505=EDGE_LOOP('',(#1223));
#553=LINE('',#2380,#609);
#554=LINE('',#2401,#610);
#555=LINE('',#2426,#611);
#556=LINE('',#2427,#612);
#557=LINE('',#2429,#613);
#558=LINE('',#2431,#614);
#559=LINE('',#2436,#615);
#560=LINE('',#2439,#616);
#561=LINE('',#2441,#617);
#609=VECTOR('',#1970,0.734027674973257);
#610=VECTOR('',#1977,0.734027674973257);
#611=VECTOR('',#1980,1.);
#612=VECTOR('',#1981,1.);
#613=VECTOR('',#1984,1.);
#614=VECTOR('',#1987,1.);
#615=VECTOR('',#1992,0.4);
#616=VECTOR('',#1997,1.);
#617=VECTOR('',#2000,1.);
#686=CIRCLE('',#1590,0.6175);
#687=CIRCLE('',#1592,0.6175);
#688=CIRCLE('',#1597,0.338975);
#689=CIRCLE('',#1598,0.338975);
#770=VERTEX_POINT('',#2370);
#771=VERTEX_POINT('',#2371);
#772=VERTEX_POINT('',#2375);
#773=VERTEX_POINT('',#2379);
#774=VERTEX_POINT('',#2382);
#775=VERTEX_POINT('',#2386);
#776=VERTEX_POINT('',#2390);
#777=VERTEX_POINT('',#2398);
#778=VERTEX_POINT('',#2400);
#779=VERTEX_POINT('',#2402);
#780=VERTEX_POINT('',#2406);
#781=VERTEX_POINT('',#2410);
#782=VERTEX_POINT('',#2414);
#783=VERTEX_POINT('',#2418);
#784=VERTEX_POINT('',#2433);
#785=VERTEX_POINT('',#2435);
#907=EDGE_CURVE('',#770,#771,#173,.T.);
#908=EDGE_CURVE('',#772,#770,#174,.T.);
#909=EDGE_CURVE('',#772,#773,#553,.T.);
#910=EDGE_CURVE('',#773,#773,#686,.T.);
#911=EDGE_CURVE('',#774,#772,#175,.T.);
#912=EDGE_CURVE('',#775,#774,#176,.T.);
#913=EDGE_CURVE('',#776,#775,#177,.T.);
#914=EDGE_CURVE('',#771,#776,#178,.T.);
#915=EDGE_CURVE('',#777,#777,#687,.T.);
#916=EDGE_CURVE('',#777,#778,#554,.T.);
#917=EDGE_CURVE('',#779,#778,#179,.T.);
#918=EDGE_CURVE('',#780,#779,#180,.T.);
#919=EDGE_CURVE('',#781,#780,#181,.T.);
#920=EDGE_CURVE('',#782,#781,#182,.T.);
#921=EDGE_CURVE('',#783,#782,#183,.T.);
#922=EDGE_CURVE('',#778,#783,#184,.T.);
#923=EDGE_CURVE('',#774,#783,#555,.T.);
#924=EDGE_CURVE('',#775,#782,#556,.T.);
#925=EDGE_CURVE('',#772,#778,#557,.T.);
#926=EDGE_CURVE('',#770,#779,#558,.T.);
#927=EDGE_CURVE('',#784,#784,#688,.F.);
#928=EDGE_CURVE('',#784,#785,#559,.T.);
#929=EDGE_CURVE('',#785,#785,#689,.F.);
#930=EDGE_CURVE('',#771,#780,#560,.T.);
#931=EDGE_CURVE('',#776,#781,#561,.T.);
#1174=ORIENTED_EDGE('',*,*,#907,.F.);
#1175=ORIENTED_EDGE('',*,*,#908,.F.);
#1176=ORIENTED_EDGE('',*,*,#909,.T.);
#1177=ORIENTED_EDGE('',*,*,#910,.F.);
#1178=ORIENTED_EDGE('',*,*,#909,.F.);
#1179=ORIENTED_EDGE('',*,*,#911,.F.);
#1180=ORIENTED_EDGE('',*,*,#912,.F.);
#1181=ORIENTED_EDGE('',*,*,#913,.F.);
#1182=ORIENTED_EDGE('',*,*,#914,.F.);
#1183=ORIENTED_EDGE('',*,*,#915,.F.);
#1184=ORIENTED_EDGE('',*,*,#916,.T.);
#1185=ORIENTED_EDGE('',*,*,#917,.F.);
#1186=ORIENTED_EDGE('',*,*,#918,.F.);
#1187=ORIENTED_EDGE('',*,*,#919,.F.);
#1188=ORIENTED_EDGE('',*,*,#920,.F.);
#1189=ORIENTED_EDGE('',*,*,#921,.F.);
#1190=ORIENTED_EDGE('',*,*,#922,.F.);
#1191=ORIENTED_EDGE('',*,*,#916,.F.);
#1192=ORIENTED_EDGE('',*,*,#912,.T.);
#1193=ORIENTED_EDGE('',*,*,#923,.T.);
#1194=ORIENTED_EDGE('',*,*,#921,.T.);
#1195=ORIENTED_EDGE('',*,*,#924,.F.);
#1196=ORIENTED_EDGE('',*,*,#911,.T.);
#1197=ORIENTED_EDGE('',*,*,#925,.T.);
#1198=ORIENTED_EDGE('',*,*,#922,.T.);
#1199=ORIENTED_EDGE('',*,*,#923,.F.);
#1200=ORIENTED_EDGE('',*,*,#908,.T.);
#1201=ORIENTED_EDGE('',*,*,#926,.T.);
#1202=ORIENTED_EDGE('',*,*,#917,.T.);
#1203=ORIENTED_EDGE('',*,*,#925,.F.);
#1204=ORIENTED_EDGE('',*,*,#927,.F.);
#1205=ORIENTED_EDGE('',*,*,#928,.T.);
#1206=ORIENTED_EDGE('',*,*,#929,.T.);
#1207=ORIENTED_EDGE('',*,*,#928,.F.);
#1208=ORIENTED_EDGE('',*,*,#907,.T.);
#1209=ORIENTED_EDGE('',*,*,#930,.T.);
#1210=ORIENTED_EDGE('',*,*,#918,.T.);
#1211=ORIENTED_EDGE('',*,*,#926,.F.);
#1212=ORIENTED_EDGE('',*,*,#913,.T.);
#1213=ORIENTED_EDGE('',*,*,#924,.T.);
#1214=ORIENTED_EDGE('',*,*,#920,.T.);
#1215=ORIENTED_EDGE('',*,*,#931,.F.);
#1216=ORIENTED_EDGE('',*,*,#914,.T.);
#1217=ORIENTED_EDGE('',*,*,#931,.T.);
#1218=ORIENTED_EDGE('',*,*,#919,.T.);
#1219=ORIENTED_EDGE('',*,*,#930,.F.);
#1220=ORIENTED_EDGE('',*,*,#915,.T.);
#1221=ORIENTED_EDGE('',*,*,#927,.T.);
#1222=ORIENTED_EDGE('',*,*,#910,.T.);
#1223=ORIENTED_EDGE('',*,*,#929,.F.);
#1257=CYLINDRICAL_SURFACE('',#1596,0.338975);
#1318=ADVANCED_FACE('',(#373),#187,.T.);
#1319=ADVANCED_FACE('',(#374),#188,.T.);
#1320=ADVANCED_FACE('',(#375),#305,.T.);
#1321=ADVANCED_FACE('',(#376),#306,.T.);
#1322=ADVANCED_FACE('',(#377),#307,.T.);
#1323=ADVANCED_FACE('',(#378),#1257,.F.);
#1324=ADVANCED_FACE('',(#379),#308,.T.);
#1325=ADVANCED_FACE('',(#380),#309,.T.);
#1326=ADVANCED_FACE('',(#381),#310,.T.);
#1327=ADVANCED_FACE('',(#382,#278),#311,.T.);
#1328=ADVANCED_FACE('',(#383,#279),#312,.F.);
#1338=CLOSED_SHELL('',(#1318,#1319,#1320,#1321,#1322,#1323,#1324,#1325,
#1326,#1327,#1328));
#1588=AXIS2_PLACEMENT_3D('',#2368,#1966,#1967);
#1589=AXIS2_PLACEMENT_3D('',#2369,#1968,#1969);
#1590=AXIS2_PLACEMENT_3D('',#2381,#1971,#1972);
#1591=AXIS2_PLACEMENT_3D('',#2397,#1973,#1974);
#1592=AXIS2_PLACEMENT_3D('',#2399,#1975,#1976);
#1593=AXIS2_PLACEMENT_3D('',#2425,#1978,#1979);
#1594=AXIS2_PLACEMENT_3D('',#2428,#1982,#1983);
#1595=AXIS2_PLACEMENT_3D('',#2430,#1985,#1986);
#1596=AXIS2_PLACEMENT_3D('',#2432,#1988,#1989);
#1597=AXIS2_PLACEMENT_3D('',#2434,#1990,#1991);
#1598=AXIS2_PLACEMENT_3D('',#2437,#1993,#1994);
#1599=AXIS2_PLACEMENT_3D('',#2438,#1995,#1996);
#1600=AXIS2_PLACEMENT_3D('',#2440,#1998,#1999);
#1601=AXIS2_PLACEMENT_3D('',#2442,#2001,#2002);
#1602=AXIS2_PLACEMENT_3D('',#2443,#2003,#2004);
#1603=AXIS2_PLACEMENT_3D('',#2444,#2005,#2006);
#1966=DIRECTION('axis',(0.,0.,1.));
#1967=DIRECTION('refdir',(1.,0.,0.));
#1968=DIRECTION('center_axis',(0.,1.,0.));
#1969=DIRECTION('ref_axis',(1.,0.,0.));
#1970=DIRECTION('',(0.866025403784439,-0.5,1.06057523872491E-16));
#1971=DIRECTION('center_axis',(0.,-1.,0.));
#1972=DIRECTION('ref_axis',(1.,0.,0.));
#1973=DIRECTION('center_axis',(0.,-1.,0.));
#1974=DIRECTION('ref_axis',(1.,0.,0.));
#1975=DIRECTION('center_axis',(0.,1.,0.));
#1976=DIRECTION('ref_axis',(1.,0.,0.));
#1977=DIRECTION('',(-0.866025403784439,-0.5,-1.06057523872491E-16));
#1978=DIRECTION('center_axis',(1.4792020664489E-16,0.,-1.));
#1979=DIRECTION('ref_axis',(-1.,0.,-1.4792020664489E-16));
#1980=DIRECTION('',(0.,1.,0.));
#1981=DIRECTION('',(0.,1.,0.));
#1982=DIRECTION('center_axis',(-0.866025403784439,0.,-0.5));
#1983=DIRECTION('ref_axis',(-0.5,0.,0.866025403784439));
#1984=DIRECTION('',(0.,1.,0.));
#1985=DIRECTION('center_axis',(-0.866025403784439,0.,0.5));
#1986=DIRECTION('ref_axis',(0.5,0.,0.866025403784439));
#1987=DIRECTION('',(0.,1.,0.));
#1988=DIRECTION('center_axis',(0.,1.,0.));
#1989=DIRECTION('ref_axis',(1.,0.,0.));
#1990=DIRECTION('center_axis',(0.,1.,0.));
#1991=DIRECTION('ref_axis',(1.,0.,0.));
#1992=DIRECTION('',(0.,-1.,0.));
#1993=DIRECTION('center_axis',(0.,1.,0.));
#1994=DIRECTION('ref_axis',(1.,0.,0.));
#1995=DIRECTION('center_axis',(-2.95840413289779E-16,0.,1.));
#1996=DIRECTION('ref_axis',(1.,0.,2.95840413289779E-16));
#1997=DIRECTION('',(0.,1.,0.));
#1998=DIRECTION('center_axis',(0.866025403784439,0.,-0.5));
#1999=DIRECTION('ref_axis',(-0.5,0.,-0.866025403784439));
#2000=DIRECTION('',(0.,1.,0.));
#2001=DIRECTION('center_axis',(0.866025403784439,0.,0.5));
#2002=DIRECTION('ref_axis',(0.5,0.,-0.866025403784439));
#2003=DIRECTION('center_axis',(0.,1.,0.));
#2004=DIRECTION('ref_axis',(1.,0.,0.));
#2005=DIRECTION('center_axis',(0.,1.,0.));
#2006=DIRECTION('ref_axis',(1.,0.,0.));
#2368=CARTESIAN_POINT('',(0.,0.,0.));
#2369=CARTESIAN_POINT('Origin',(0.,0.067277284513851,0.));
#2370=CARTESIAN_POINT('',(-0.375277674973257,0.0768195421087395,0.65));
#2371=CARTESIAN_POINT('',(0.375277674973257,0.0768195421087395,0.65));
#2372=CARTESIAN_POINT('Ctrl Pts',(-0.375277674973257,0.0768195421087395,
0.65));
#2373=CARTESIAN_POINT('Ctrl Pts',(1.66533453693773E-13,-0.0315137912242439,
0.65));
#2374=CARTESIAN_POINT('Ctrl Pts',(0.375277674973257,0.0768195421087394,
0.65));
#2375=CARTESIAN_POINT('',(-0.750555349946514,0.0768195421087394,-9.19165206894919E-17));
#2376=CARTESIAN_POINT('Ctrl Pts',(-0.750555349946514,0.0768195421087394,
-9.19165206894919E-17));
#2377=CARTESIAN_POINT('Ctrl Pts',(-0.562916512459802,-0.0315137912242434,
0.325000000000144));
#2378=CARTESIAN_POINT('Ctrl Pts',(-0.375277674973257,0.0768195421087395,
0.65));
#2379=CARTESIAN_POINT('',(-0.6175,-2.77555756156289E-17,-7.5621939847349E-17));
#2380=CARTESIAN_POINT('',(-0.734027674973257,0.067277284513851,-8.98924642641573E-17));
#2381=CARTESIAN_POINT('Origin',(0.,0.,0.));
#2382=CARTESIAN_POINT('',(-0.375277674973257,0.0768195421087395,-0.65));
#2383=CARTESIAN_POINT('Ctrl Pts',(-0.375277674973257,0.0768195421087395,
-0.65));
#2384=CARTESIAN_POINT('Ctrl Pts',(-0.562916512459968,-0.0315137912242437,
-0.324999999999856));
#2385=CARTESIAN_POINT('Ctrl Pts',(-0.750555349946514,0.0768195421087395,
-9.19165206894919E-17));
#2386=CARTESIAN_POINT('',(0.375277674973257,0.0768195421087395,-0.65));
#2387=CARTESIAN_POINT('Ctrl Pts',(0.375277674973257,0.0768195421087395,
-0.65));
#2388=CARTESIAN_POINT('Ctrl Pts',(-1.66144875635155E-13,-0.0315137912242437,
-0.65));
#2389=CARTESIAN_POINT('Ctrl Pts',(-0.375277674973257,0.0768195421087395,
-0.65));
#2390=CARTESIAN_POINT('',(0.750555349946514,0.0768195421087394,0.));
#2391=CARTESIAN_POINT('Ctrl Pts',(0.750555349946514,0.0768195421087394,
0.));
#2392=CARTESIAN_POINT('Ctrl Pts',(0.562916512459802,-0.0315137912242436,
-0.325000000000144));
#2393=CARTESIAN_POINT('Ctrl Pts',(0.375277674973257,0.0768195421087395,
-0.65));
#2394=CARTESIAN_POINT('Ctrl Pts',(0.375277674973257,0.0768195421087394,
0.65));
#2395=CARTESIAN_POINT('Ctrl Pts',(0.562916512459968,-0.0315137912242439,
0.324999999999856));
#2396=CARTESIAN_POINT('Ctrl Pts',(0.750555349946514,0.0768195421087394,
0.));
#2397=CARTESIAN_POINT('Origin',(0.,0.612722715486149,0.));
#2398=CARTESIAN_POINT('',(-0.6175,0.68,-7.5621939847349E-17));
#2399=CARTESIAN_POINT('Origin',(0.,0.68,0.));
#2400=CARTESIAN_POINT('',(-0.750555349946514,0.603180457891261,-9.19165206894919E-17));
#2401=CARTESIAN_POINT('',(-0.734027674973257,0.612722715486149,-8.98924642641573E-17));
#2402=CARTESIAN_POINT('',(-0.375277674973257,0.603180457891261,0.65));
#2403=CARTESIAN_POINT('Ctrl Pts',(-0.375277674973257,0.603180457891261,
0.65));
#2404=CARTESIAN_POINT('Ctrl Pts',(-0.562916512459968,0.711513791224243,
0.324999999999856));
#2405=CARTESIAN_POINT('Ctrl Pts',(-0.750555349946514,0.603180457891261,
-9.19165206894919E-17));
#2406=CARTESIAN_POINT('',(0.375277674973257,0.603180457891261,0.65));
#2407=CARTESIAN_POINT('Ctrl Pts',(0.375277674973257,0.603180457891261,0.65));
#2408=CARTESIAN_POINT('Ctrl Pts',(-1.66755498298699E-13,0.711513791224244,
0.65));
#2409=CARTESIAN_POINT('Ctrl Pts',(-0.375277674973257,0.603180457891261,
0.65));
#2410=CARTESIAN_POINT('',(0.750555349946514,0.603180457891261,0.));
#2411=CARTESIAN_POINT('Ctrl Pts',(0.750555349946514,0.603180457891261,0.));
#2412=CARTESIAN_POINT('Ctrl Pts',(0.562916512459802,0.711513791224244,0.325000000000144));
#2413=CARTESIAN_POINT('Ctrl Pts',(0.375277674973257,0.603180457891261,0.65));
#2414=CARTESIAN_POINT('',(0.375277674973257,0.603180457891261,-0.65));
#2415=CARTESIAN_POINT('Ctrl Pts',(0.375277674973257,0.603180457891261,-0.65));
#2416=CARTESIAN_POINT('Ctrl Pts',(0.562916512459969,0.711513791224244,-0.324999999999856));
#2417=CARTESIAN_POINT('Ctrl Pts',(0.750555349946514,0.603180457891261,0.));
#2418=CARTESIAN_POINT('',(-0.375277674973257,0.603180457891261,-0.65));
#2419=CARTESIAN_POINT('Ctrl Pts',(-0.375277674973257,0.603180457891261,
-0.65));
#2420=CARTESIAN_POINT('Ctrl Pts',(1.66422431391311E-13,0.711513791224244,
-0.65));
#2421=CARTESIAN_POINT('Ctrl Pts',(0.375277674973257,0.603180457891261,-0.65));
#2422=CARTESIAN_POINT('Ctrl Pts',(-0.750555349946514,0.603180457891261,
-9.19165206894919E-17));
#2423=CARTESIAN_POINT('Ctrl Pts',(-0.562916512459802,0.711513791224244,
-0.325000000000144));
#2424=CARTESIAN_POINT('Ctrl Pts',(-0.375277674973257,0.603180457891261,
-0.65));
#2425=CARTESIAN_POINT('Origin',(0.375277674973257,0.,-0.65));
#2426=CARTESIAN_POINT('',(-0.375277674973257,0.,-0.65));
#2427=CARTESIAN_POINT('',(0.375277674973257,0.,-0.65));
#2428=CARTESIAN_POINT('Origin',(-0.375277674973257,0.,-0.65));
#2429=CARTESIAN_POINT('',(-0.750555349946514,0.,-9.19165206894919E-17));
#2430=CARTESIAN_POINT('Origin',(-0.750555349946514,0.,-9.19165206894919E-17));
#2431=CARTESIAN_POINT('',(-0.375277674973257,0.,0.65));
#2432=CARTESIAN_POINT('Origin',(0.,0.,0.));
#2433=CARTESIAN_POINT('',(-0.338975,0.68,4.15124648740974E-17));
#2434=CARTESIAN_POINT('Origin',(0.,0.68,0.));
#2435=CARTESIAN_POINT('',(-0.338975,0.,4.15124648740974E-17));
#2436=CARTESIAN_POINT('',(-0.338975,0.,4.15124648740974E-17));
#2437=CARTESIAN_POINT('Origin',(0.,0.,0.));
#2438=CARTESIAN_POINT('Origin',(-0.375277674973257,0.,0.65));
#2439=CARTESIAN_POINT('',(0.375277674973257,0.,0.65));
#2440=CARTESIAN_POINT('Origin',(0.750555349946514,0.,0.));
#2441=CARTESIAN_POINT('',(0.750555349946514,0.,0.));
#2442=CARTESIAN_POINT('Origin',(0.375277674973257,0.,0.65));
#2443=CARTESIAN_POINT('Origin',(0.,0.68,-1.11022302462516E-16));
#2444=CARTESIAN_POINT('Origin',(0.,0.,-1.11022302462516E-16));
#2494=UNCERTAINTY_MEASURE_WITH_UNIT(LENGTH_MEASURE(0.001),#2508,
'DISTANCE_ACCURACY_VALUE',
'Maximum model space distance between geometric entities at asserted c
onnectivities');
#2495=UNCERTAINTY_MEASURE_WITH_UNIT(LENGTH_MEASURE(0.001),#2508,
'DISTANCE_ACCURACY_VALUE',
'Maximum model space distance between geometric entities at asserted c
onnectivities');
#2506=(
GEOMETRIC_REPRESENTATION_CONTEXT(3)
GLOBAL_UNCERTAINTY_ASSIGNED_CONTEXT((#2494))
GLOBAL_UNIT_ASSIGNED_CONTEXT((#2508,#2510,#2511))
REPRESENTATION_CONTEXT('','3D')
);
#2507=(
GEOMETRIC_REPRESENTATION_CONTEXT(3)
GLOBAL_UNCERTAINTY_ASSIGNED_CONTEXT((#2495))
GLOBAL_UNIT_ASSIGNED_CONTEXT((#2508,#2510,#2511))
REPRESENTATION_CONTEXT('','3D')
);
#2508=(
LENGTH_UNIT()
NAMED_UNIT(*)
SI_UNIT(.CENTI.,.METRE.)
);
#2510=(
NAMED_UNIT(*)
PLANE_ANGLE_UNIT()
SI_UNIT($,.RADIAN.)
);
#2511=(
NAMED_UNIT(*)
SI_UNIT($,.STERADIAN.)
SOLID_ANGLE_UNIT()
);
#2522=SHAPE_DEFINITION_REPRESENTATION(#2533,#2583);
#2533=PRODUCT_DEFINITION_SHAPE('',$,#2595);
#2583=SHAPE_REPRESENTATION('',(#1588),#2506);
#2584=PRODUCT_DEFINITION_CONTEXT('part definition',#2619,'design');
#2595=PRODUCT_DEFINITION('Hex Nut - M8','Hex Nut - M8',#2606,
#2584);
#2606=PRODUCT_DEFINITION_FORMATION('',$,#2631);
#2619=APPLICATION_CONTEXT(
'Core Data for Automotive Mechanical Design Process');
#2620=PRODUCT_CONTEXT('part definition',#2619,'mechanical');
#2631=PRODUCT('Hex Nut - M8','Hex Nut - M8','Hex Nut - M8',
(#2620));
#2695=COLOUR_RGB('Black',0.12,0.14,0.17);
#2696=FILL_AREA_STYLE_COLOUR('',#2695);
#2697=FILL_AREA_STYLE('',(#2696));
#2698=SURFACE_STYLE_FILL_AREA(#2697);
#2699=SURFACE_SIDE_STYLE('',(#2698));
#2700=SURFACE_STYLE_USAGE(.BOTH.,#2699);
#2701=PRESENTATION_STYLE_ASSIGNMENT((#2700));
ENDSEC;
END-ISO-10303-21;
